ISO-10303-21;
HEADER;
/* Generated by software containing ST-Developer
 * from STEP Tools, Inc. (www.steptools.com) 
 */
/* OPTION: using custom renumber hook */

FILE_DESCRIPTION(
/* description */ ('STEP AP242 Edition 2', 'CAx-IF Rec.Pracs.---Representation and Presentation of Product Manufa
cturing Information (PMI)---4.0---2014-10-13', 'CAx-IF Rec.Pracs.---3D Tessellated Geometry---0.4---2014-09-14', '2;1', 'CAx-IF Rec.Pracs.---User Defined Attributes---1.5---2016-08-15'),
/* implementation_level */ '2;1');

FILE_NAME(
/* name */ 'endcap2__ DE    22113.step',
/* time_stamp */ '2026-10-09T00:23:50Z',
/* author */ (''),
/* organization */ (''),
/* preprocessor_version */ 'ST-DEVELOPER v20',
/* originating_system */ 'ONSHAPE BY PTC INC, 1.221',
/* authorisation */ '  ');

FILE_SCHEMA (('AP242_MANAGED_MODEL_BASED_3D_ENGINEERING_MIM_LF { 1 0 10303 442 3 1 4 }'));
ENDSEC;

DATA;
#23=CONICAL_SURFACE('',#8568,0.,0.78539816339745);
#34=TOROIDAL_SURFACE('',#8549,0.00799999999990077,0.000500000000345792);
#35=TOROIDAL_SURFACE('',#8551,0.0119999999999008,0.000500000000345788);
#36=TOROIDAL_SURFACE('',#8555,0.00799999999990077,0.00050000000034579);
#37=TOROIDAL_SURFACE('',#8561,0.00950000000009923,0.000500000000345799);
#38=TOROIDAL_SURFACE('',#8563,0.00849999999905548,0.000499999999472932);
#39=TOROIDAL_SURFACE('',#8564,0.00849999999905548,0.000499999999472929);
#40=TOROIDAL_SURFACE('',#8570,0.00799999999935485,0.00100000000059717);
#41=TOROIDAL_SURFACE('',#8572,0.00799999999935485,0.00100000000059717);
#42=TOROIDAL_SURFACE('',#8573,0.00800000000094452,0.000499999999472942);
#43=TOROIDAL_SURFACE('',#8574,0.00800000000094452,0.000499999999472943);
#144=SHAPE_REPRESENTATION_RELATIONSHIP('','',#8234,#150);
#150=ADVANCED_BREP_SHAPE_REPRESENTATION('',(#8220),#18812);
#475=B_SPLINE_CURVE_WITH_KNOTS('',3,(#12986,#12987,#12988,#12989,#12990,
#12991,#12992,#12993,#12994,#12995,#12996),.UNSPECIFIED.,.F.,.F.,(4,1,1,
1,1,1,1,1,4),(1.82133646569706E-10,0.125000000151206,0.250000000120279,
0.375000000089351,0.500000000058424,0.625000000027496,0.749999999996569,
0.874999999965641,0.999999999934714),.UNSPECIFIED.);
#476=B_SPLINE_CURVE_WITH_KNOTS('',3,(#13001,#13002,#13003,#13004,#13005,
#13006,#13007,#13008,#13009,#13010,#13011),.UNSPECIFIED.,.F.,.F.,(4,1,1,
1,1,1,1,1,4),(0.,0.125,0.25,0.375,0.5,0.625,0.75,0.875,1.),
 .UNSPECIFIED.);
#477=B_SPLINE_CURVE_WITH_KNOTS('',3,(#13016,#13017,#13018,#13019,#13020,
#13021,#13022),.UNSPECIFIED.,.F.,.F.,(4,1,1,1,4),(1.08159974291989E-10,
0.250000000064798,0.500000000021436,0.749999999978074,0.999999999934712),
 .UNSPECIFIED.);
#478=B_SPLINE_CURVE_WITH_KNOTS('',3,(#13030,#13031,#13032,#13033,#13034,
#13035,#13036),.UNSPECIFIED.,.F.,.F.,(4,1,1,1,4),(0.,0.25,0.5,0.75,1.),
 .UNSPECIFIED.);
#479=B_SPLINE_CURVE_WITH_KNOTS('',3,(#13044,#13045,#13046,#13047,#13048,
#13049,#13050,#13051,#13052,#13053,#13054),.UNSPECIFIED.,.F.,.F.,(4,1,1,
1,1,1,1,1,4),(4.32086807808983E-11,0.125000000029647,0.250000000016085,
0.375000000002522,0.49999999998896,0.624999999975398,0.749999999961836,
0.874999999948274,0.999999999934712),.UNSPECIFIED.);
#480=B_SPLINE_CURVE_WITH_KNOTS('',3,(#13056,#13057,#13058,#13059),
 .UNSPECIFIED.,.F.,.F.,(4,4),(0.,1.),.UNSPECIFIED.);
#481=B_SPLINE_CURVE_WITH_KNOTS('',3,(#13061,#13062,#13063,#13064,#13065,
#13066,#13067),.UNSPECIFIED.,.F.,.F.,(4,1,1,1,4),(6.52880993013389E-11,
0.250000000020525,0.499999999975762,0.749999999930999,0.999999999886236),
 .UNSPECIFIED.);
#482=B_SPLINE_CURVE_WITH_KNOTS('',3,(#13069,#13070,#13071,#13072),
 .UNSPECIFIED.,.F.,.F.,(4,4),(0.,1.),.UNSPECIFIED.);
#483=B_SPLINE_CURVE_WITH_KNOTS('',3,(#13076,#13077,#13078,#13079,#13080,
#13081,#13082,#13083,#13084,#13085,#13086),.UNSPECIFIED.,.F.,.F.,(4,1,1,
1,1,1,1,1,4),(0.,0.125,0.25,0.375,0.5,0.625,0.75,0.875,1.),
 .UNSPECIFIED.);
#484=B_SPLINE_CURVE_WITH_KNOTS('',3,(#13094,#13095,#13096,#13097,#13098,
#13099,#13100,#13101,#13102,#13103,#13104),.UNSPECIFIED.,.F.,.F.,(4,1,1,
1,1,1,1,1,4),(0.,0.125,0.25,0.375,0.5,0.625,0.75,0.875,1.),
 .UNSPECIFIED.);
#485=B_SPLINE_CURVE_WITH_KNOTS('',3,(#13106,#13107,#13108,#13109),
 .UNSPECIFIED.,.F.,.F.,(4,4),(0.,1.),.UNSPECIFIED.);
#486=B_SPLINE_CURVE_WITH_KNOTS('',3,(#13113,#13114,#13115,#13116),
 .UNSPECIFIED.,.F.,.F.,(4,4),(0.,1.),.UNSPECIFIED.);
#487=B_SPLINE_CURVE_WITH_KNOTS('',3,(#13118,#13119,#13120,#13121,#13122,
#13123,#13124,#13125,#13126,#13127,#13128),.UNSPECIFIED.,.F.,.F.,(4,1,1,
1,1,1,1,1,4),(6.52871450848788E-11,0.125000000057126,0.250000000048965,
0.375000000040805,0.500000000032644,0.625000000024483,0.750000000016322,
0.875000000008161,1.),.UNSPECIFIED.);
#488=B_SPLINE_CURVE_WITH_KNOTS('',3,(#13130,#13131,#13132,#13133),
 .UNSPECIFIED.,.F.,.F.,(4,4),(0.,1.),.UNSPECIFIED.);
#489=B_SPLINE_CURVE_WITH_KNOTS('',3,(#13135,#13136,#13137,#13138,#13139,
#13140,#13141,#13142,#13143,#13144,#13145),.UNSPECIFIED.,.F.,.F.,(4,1,1,
1,1,1,1,1,4),(7.9578112254039E-11,0.12500000006147,0.250000000043362,0.375000000025254,
0.500000000007146,0.624999999989038,0.74999999997093,0.874999999952822,
0.999999999934714),.UNSPECIFIED.);
#490=B_SPLINE_CURVE_WITH_KNOTS('',3,(#13147,#13148,#13149,#13150),
 .UNSPECIFIED.,.F.,.F.,(4,4),(0.,1.),.UNSPECIFIED.);
#1033=PLANE('',#8545);
#1034=PLANE('',#8547);
#1035=PLANE('',#8557);
#1994=ORIENTED_EDGE('',*,*,#3918,.F.);
#1995=ORIENTED_EDGE('',*,*,#3919,.F.);
#1996=ORIENTED_EDGE('',*,*,#3920,.F.);
#1997=ORIENTED_EDGE('',*,*,#3918,.T.);
#1998=ORIENTED_EDGE('',*,*,#3921,.F.);
#1999=ORIENTED_EDGE('',*,*,#3919,.T.);
#2000=ORIENTED_EDGE('',*,*,#3922,.T.);
#2001=ORIENTED_EDGE('',*,*,#3923,.T.);
#2002=ORIENTED_EDGE('',*,*,#3920,.T.);
#2003=ORIENTED_EDGE('',*,*,#3921,.T.);
#2004=ORIENTED_EDGE('',*,*,#3924,.T.);
#2005=ORIENTED_EDGE('',*,*,#3922,.F.);
#2006=ORIENTED_EDGE('',*,*,#3923,.F.);
#2007=ORIENTED_EDGE('',*,*,#3925,.T.);
#2008=ORIENTED_EDGE('',*,*,#3926,.T.);
#2009=ORIENTED_EDGE('',*,*,#3926,.F.);
#2010=ORIENTED_EDGE('',*,*,#3925,.F.);
#2011=ORIENTED_EDGE('',*,*,#3927,.T.);
#2012=ORIENTED_EDGE('',*,*,#3928,.T.);
#2013=ORIENTED_EDGE('',*,*,#3924,.F.);
#2014=ORIENTED_EDGE('',*,*,#3929,.F.);
#2015=ORIENTED_EDGE('',*,*,#3928,.F.);
#2016=ORIENTED_EDGE('',*,*,#3927,.F.);
#2017=ORIENTED_EDGE('',*,*,#3930,.T.);
#2018=ORIENTED_EDGE('',*,*,#3931,.T.);
#2019=ORIENTED_EDGE('',*,*,#3932,.F.);
#2020=ORIENTED_EDGE('',*,*,#3933,.F.);
#2021=ORIENTED_EDGE('',*,*,#3929,.T.);
#2022=ORIENTED_EDGE('',*,*,#3934,.F.);
#2023=ORIENTED_EDGE('',*,*,#3935,.F.);
#2024=ORIENTED_EDGE('',*,*,#3936,.F.);
#2025=ORIENTED_EDGE('',*,*,#3930,.F.);
#2026=ORIENTED_EDGE('',*,*,#3931,.F.);
#2027=ORIENTED_EDGE('',*,*,#3936,.T.);
#2028=ORIENTED_EDGE('',*,*,#3937,.F.);
#2029=ORIENTED_EDGE('',*,*,#3934,.T.);
#2030=ORIENTED_EDGE('',*,*,#3938,.T.);
#2031=ORIENTED_EDGE('',*,*,#3939,.T.);
#2032=ORIENTED_EDGE('',*,*,#3932,.T.);
#2033=ORIENTED_EDGE('',*,*,#3933,.T.);
#2034=ORIENTED_EDGE('',*,*,#3940,.T.);
#2035=ORIENTED_EDGE('',*,*,#3941,.T.);
#2036=ORIENTED_EDGE('',*,*,#3935,.T.);
#2037=ORIENTED_EDGE('',*,*,#3937,.T.);
#2038=ORIENTED_EDGE('',*,*,#3939,.F.);
#2039=ORIENTED_EDGE('',*,*,#3942,.T.);
#2040=ORIENTED_EDGE('',*,*,#3943,.T.);
#2041=ORIENTED_EDGE('',*,*,#3944,.T.);
#2042=ORIENTED_EDGE('',*,*,#3942,.F.);
#2043=ORIENTED_EDGE('',*,*,#3938,.F.);
#2044=ORIENTED_EDGE('',*,*,#3944,.F.);
#2045=ORIENTED_EDGE('',*,*,#3945,.T.);
#2046=ORIENTED_EDGE('',*,*,#3946,.T.);
#2047=ORIENTED_EDGE('',*,*,#3947,.T.);
#2048=ORIENTED_EDGE('',*,*,#3948,.T.);
#2049=ORIENTED_EDGE('',*,*,#3941,.F.);
#2050=ORIENTED_EDGE('',*,*,#3949,.T.);
#2051=ORIENTED_EDGE('',*,*,#3946,.F.);
#2052=ORIENTED_EDGE('',*,*,#3940,.F.);
#2053=ORIENTED_EDGE('',*,*,#3948,.F.);
#2054=ORIENTED_EDGE('',*,*,#3947,.F.);
#2055=ORIENTED_EDGE('',*,*,#3949,.F.);
#2056=ORIENTED_EDGE('',*,*,#3943,.F.);
#2057=ORIENTED_EDGE('',*,*,#3945,.F.);
#3918=EDGE_CURVE('',#4945,#4945,#5629,.F.);
#3919=EDGE_CURVE('',#4946,#4946,#5630,.T.);
#3920=EDGE_CURVE('',#4947,#4947,#5631,.F.);
#3921=EDGE_CURVE('',#4948,#4948,#5632,.T.);
#3922=EDGE_CURVE('',#4949,#4950,#5633,.T.);
#3923=EDGE_CURVE('',#4950,#4949,#475,.T.);
#3924=EDGE_CURVE('',#4951,#4951,#5634,.F.);
#3925=EDGE_CURVE('',#4952,#4953,#476,.F.);
#3926=EDGE_CURVE('',#4953,#4952,#5635,.F.);
#3927=EDGE_CURVE('',#4954,#4955,#477,.T.);
#3928=EDGE_CURVE('',#4955,#4954,#5636,.T.);
#3929=EDGE_CURVE('',#4956,#4956,#5637,.T.);
#3930=EDGE_CURVE('',#4957,#4958,#478,.F.);
#3931=EDGE_CURVE('',#4958,#4957,#5638,.F.);
#3932=EDGE_CURVE('',#4959,#4960,#5639,.F.);
#3933=EDGE_CURVE('',#4960,#4959,#479,.T.);
#3934=EDGE_CURVE('',#4961,#4957,#480,.T.);
#3935=EDGE_CURVE('',#4962,#4961,#481,.T.);
#3936=EDGE_CURVE('',#4958,#4962,#482,.T.);
#3937=EDGE_CURVE('',#4961,#4962,#5640,.T.);
#3938=EDGE_CURVE('',#4963,#4964,#483,.F.);
#3939=EDGE_CURVE('',#4964,#4963,#5641,.T.);
#3940=EDGE_CURVE('',#4965,#4966,#5642,.F.);
#3941=EDGE_CURVE('',#4966,#4965,#484,.F.);
#3942=EDGE_CURVE('',#4964,#4967,#485,.T.);
#3943=EDGE_CURVE('',#4967,#4968,#5643,.F.);
#3944=EDGE_CURVE('',#4968,#4963,#486,.T.);
#3945=EDGE_CURVE('',#4968,#4967,#487,.T.);
#3946=EDGE_CURVE('',#4966,#4969,#488,.T.);
#3947=EDGE_CURVE('',#4969,#4970,#489,.T.);
#3948=EDGE_CURVE('',#4970,#4965,#490,.T.);
#3949=EDGE_CURVE('',#4970,#4969,#5644,.T.);
#4945=VERTEX_POINT('',#12973);
#4946=VERTEX_POINT('',#12975);
#4947=VERTEX_POINT('',#12978);
#4948=VERTEX_POINT('',#12981);
#4949=VERTEX_POINT('',#12984);
#4950=VERTEX_POINT('',#12985);
#4951=VERTEX_POINT('',#12999);
#4952=VERTEX_POINT('',#13012);
#4953=VERTEX_POINT('',#13013);
#4954=VERTEX_POINT('',#13023);
#4955=VERTEX_POINT('',#13024);
#4956=VERTEX_POINT('',#13028);
#4957=VERTEX_POINT('',#13037);
#4958=VERTEX_POINT('',#13038);
#4959=VERTEX_POINT('',#13042);
#4960=VERTEX_POINT('',#13043);
#4961=VERTEX_POINT('',#13060);
#4962=VERTEX_POINT('',#13068);
#4963=VERTEX_POINT('',#13087);
#4964=VERTEX_POINT('',#13088);
#4965=VERTEX_POINT('',#13092);
#4966=VERTEX_POINT('',#13093);
#4967=VERTEX_POINT('',#13110);
#4968=VERTEX_POINT('',#13112);
#4969=VERTEX_POINT('',#13134);
#4970=VERTEX_POINT('',#13146);
#5629=CIRCLE('',#8543,0.0075);
#5630=CIRCLE('',#8544,0.0075);
#5631=CIRCLE('',#8546,0.00800000000055703);
#5632=CIRCLE('',#8548,0.012000000000557);
#5633=CIRCLE('',#8550,0.00850000000024656);
#5634=CIRCLE('',#8552,0.012000000000557);
#5635=CIRCLE('',#8554,0.0085);
#5636=CIRCLE('',#8556,0.00800000000055703);
#5637=CIRCLE('',#8558,0.00949999999944297);
#5638=CIRCLE('',#8560,0.008);
#5639=CIRCLE('',#8562,0.009);
#5640=CIRCLE('',#8565,0.00814644660912898);
#5641=CIRCLE('',#8567,0.009);
#5642=CIRCLE('',#8569,0.00835355339112897);
#5643=CIRCLE('',#8571,0.0085000000001643);
#5644=CIRCLE('',#8575,0.00850000000041746);
#6135=EDGE_LOOP('',(#1994));
#6136=EDGE_LOOP('',(#1995));
#6137=EDGE_LOOP('',(#1996));
#6138=EDGE_LOOP('',(#1997));
#6139=EDGE_LOOP('',(#1998));
#6140=EDGE_LOOP('',(#1999));
#6141=EDGE_LOOP('',(#2000,#2001));
#6142=EDGE_LOOP('',(#2002));
#6143=EDGE_LOOP('',(#2003));
#6144=EDGE_LOOP('',(#2004));
#6145=EDGE_LOOP('',(#2005,#2006));
#6146=EDGE_LOOP('',(#2007,#2008));
#6147=EDGE_LOOP('',(#2009,#2010));
#6148=EDGE_LOOP('',(#2011,#2012));
#6149=EDGE_LOOP('',(#2013));
#6150=EDGE_LOOP('',(#2014));
#6151=EDGE_LOOP('',(#2015,#2016));
#6152=EDGE_LOOP('',(#2017,#2018));
#6153=EDGE_LOOP('',(#2019,#2020));
#6154=EDGE_LOOP('',(#2021));
#6155=EDGE_LOOP('',(#2022,#2023,#2024,#2025));
#6156=EDGE_LOOP('',(#2026,#2027,#2028,#2029));
#6157=EDGE_LOOP('',(#2030,#2031));
#6158=EDGE_LOOP('',(#2032,#2033));
#6159=EDGE_LOOP('',(#2034,#2035));
#6160=EDGE_LOOP('',(#2036,#2037));
#6161=EDGE_LOOP('',(#2038,#2039,#2040,#2041));
#6162=EDGE_LOOP('',(#2042,#2043,#2044,#2045));
#6163=EDGE_LOOP('',(#2046,#2047,#2048,#2049));
#6164=EDGE_LOOP('',(#2050,#2051,#2052,#2053));
#6165=EDGE_LOOP('',(#2054,#2055));
#6166=EDGE_LOOP('',(#2056,#2057));
#6896=FACE_BOUND('',#6135,.T.);
#6897=FACE_BOUND('',#6136,.T.);
#6898=FACE_BOUND('',#6137,.T.);
#6899=FACE_BOUND('',#6138,.T.);
#6900=FACE_BOUND('',#6139,.T.);
#6901=FACE_BOUND('',#6140,.T.);
#6902=FACE_BOUND('',#6141,.T.);
#6903=FACE_BOUND('',#6142,.T.);
#6904=FACE_BOUND('',#6143,.T.);
#6905=FACE_BOUND('',#6144,.T.);
#6906=FACE_BOUND('',#6145,.T.);
#6907=FACE_BOUND('',#6146,.T.);
#6908=FACE_BOUND('',#6147,.T.);
#6909=FACE_BOUND('',#6148,.T.);
#6910=FACE_BOUND('',#6149,.T.);
#6911=FACE_BOUND('',#6150,.T.);
#6912=FACE_BOUND('',#6151,.T.);
#6913=FACE_BOUND('',#6152,.T.);
#6914=FACE_BOUND('',#6153,.T.);
#6915=FACE_BOUND('',#6154,.T.);
#6916=FACE_BOUND('',#6155,.T.);
#6917=FACE_BOUND('',#6156,.T.);
#6918=FACE_BOUND('',#6157,.T.);
#6919=FACE_BOUND('',#6158,.T.);
#6920=FACE_BOUND('',#6159,.T.);
#6921=FACE_BOUND('',#6160,.T.);
#6922=FACE_BOUND('',#6161,.T.);
#6923=FACE_BOUND('',#6162,.T.);
#6924=FACE_BOUND('',#6163,.T.);
#6925=FACE_BOUND('',#6164,.T.);
#6926=FACE_BOUND('',#6165,.T.);
#6927=FACE_BOUND('',#6166,.T.);
#7501=CYLINDRICAL_SURFACE('',#8542,0.0075);
#7502=CYLINDRICAL_SURFACE('',#8553,0.0085);
#7503=CYLINDRICAL_SURFACE('',#8559,0.008);
#7504=CYLINDRICAL_SURFACE('',#8566,0.009);
#7505=CYLINDRICAL_SURFACE('',#8576,0.0085);
#7835=ADVANCED_FACE('',(#6896,#6897),#7501,.F.);
#7836=ADVANCED_FACE('',(#6898,#6899),#1033,.F.);
#7837=ADVANCED_FACE('',(#6900,#6901),#1034,.F.);
#7838=ADVANCED_FACE('',(#6902,#6903),#34,.T.);
#7839=ADVANCED_FACE('',(#6904,#6905),#35,.T.);
#7840=ADVANCED_FACE('',(#6906,#6907),#7502,.T.);
#7841=ADVANCED_FACE('',(#6908,#6909),#36,.T.);
#7842=ADVANCED_FACE('',(#6910,#6911),#1035,.F.);
#7843=ADVANCED_FACE('',(#6912,#6913),#7503,.T.);
#7844=ADVANCED_FACE('',(#6914,#6915),#37,.F.);
#7845=ADVANCED_FACE('',(#6916),#38,.F.);
#7846=ADVANCED_FACE('',(#6917),#39,.F.);
#7847=ADVANCED_FACE('',(#6918,#6919),#7504,.T.);
#7848=ADVANCED_FACE('',(#6920,#6921),#23,.T.);
#7849=ADVANCED_FACE('',(#6922),#40,.T.);
#7850=ADVANCED_FACE('',(#6923),#41,.T.);
#7851=ADVANCED_FACE('',(#6924),#42,.T.);
#7852=ADVANCED_FACE('',(#6925),#43,.T.);
#7853=ADVANCED_FACE('',(#6926,#6927),#7505,.T.);
#8169=CLOSED_SHELL('',(#7835,#7836,#7837,#7838,#7839,#7840,#7841,#7842,
#7843,#7844,#7845,#7846,#7847,#7848,#7849,#7850,#7851,#7852,#7853));
#8175=STYLED_ITEM('',(#8181),#8220);
#8181=PRESENTATION_STYLE_ASSIGNMENT((#8187));
#8187=SURFACE_STYLE_USAGE(.BOTH.,#8193);
#8193=SURFACE_SIDE_STYLE('',(#8199));
#8199=SURFACE_STYLE_FILL_AREA(#8205);
#8205=FILL_AREA_STYLE('',(#8211));
#8211=FILL_AREA_STYLE_COLOUR('',#8216);
#8216=COLOUR_RGB('', 0.66274510, 0.83137255, 0.94901961);
#8220=MANIFOLD_SOLID_BREP('endcap2__ DE    22113',#8169);
#8227=SHAPE_DEFINITION_REPRESENTATION(#18830,#8234);
#8234=SHAPE_REPRESENTATION('endcap2__ DE    22113',(#8239),#18812);
#8239=AXIS2_PLACEMENT_3D('',#11098,#9192,#9193);
#8542=AXIS2_PLACEMENT_3D('',#12971,#9798,#9799);
#8543=AXIS2_PLACEMENT_3D('',#12972,#9800,#9801);
#8544=AXIS2_PLACEMENT_3D('',#12974,#9802,#9803);
#8545=AXIS2_PLACEMENT_3D('',#12976,#9804,#9805);
#8546=AXIS2_PLACEMENT_3D('',#12977,#9806,#9807);
#8547=AXIS2_PLACEMENT_3D('',#12979,#9808,#9809);
#8548=AXIS2_PLACEMENT_3D('',#12980,#9810,#9811);
#8549=AXIS2_PLACEMENT_3D('',#12982,#9812,#9813);
#8550=AXIS2_PLACEMENT_3D('',#12983,#9814,#9815);
#8551=AXIS2_PLACEMENT_3D('',#12997,#9816,#9817);
#8552=AXIS2_PLACEMENT_3D('',#12998,#9818,#9819);
#8553=AXIS2_PLACEMENT_3D('',#13000,#9820,#9821);
#8554=AXIS2_PLACEMENT_3D('',#13014,#9822,#9823);
#8555=AXIS2_PLACEMENT_3D('',#13015,#9824,#9825);
#8556=AXIS2_PLACEMENT_3D('',#13025,#9826,#9827);
#8557=AXIS2_PLACEMENT_3D('',#13026,#9828,#9829);
#8558=AXIS2_PLACEMENT_3D('',#13027,#9830,#9831);
#8559=AXIS2_PLACEMENT_3D('',#13029,#9832,#9833);
#8560=AXIS2_PLACEMENT_3D('',#13039,#9834,#9835);
#8561=AXIS2_PLACEMENT_3D('',#13040,#9836,#9837);
#8562=AXIS2_PLACEMENT_3D('',#13041,#9838,#9839);
#8563=AXIS2_PLACEMENT_3D('',#13055,#9840,#9841);
#8564=AXIS2_PLACEMENT_3D('',#13073,#9842,#9843);
#8565=AXIS2_PLACEMENT_3D('',#13074,#9844,#9845);
#8566=AXIS2_PLACEMENT_3D('',#13075,#9846,#9847);
#8567=AXIS2_PLACEMENT_3D('',#13089,#9848,#9849);
#8568=AXIS2_PLACEMENT_3D('',#13090,#9850,#9851);
#8569=AXIS2_PLACEMENT_3D('',#13091,#9852,#9853);
#8570=AXIS2_PLACEMENT_3D('',#13105,#9854,#9855);
#8571=AXIS2_PLACEMENT_3D('',#13111,#9856,#9857);
#8572=AXIS2_PLACEMENT_3D('',#13117,#9858,#9859);
#8573=AXIS2_PLACEMENT_3D('',#13129,#9860,#9861);
#8574=AXIS2_PLACEMENT_3D('',#13151,#9862,#9863);
#8575=AXIS2_PLACEMENT_3D('',#13152,#9864,#9865);
#8576=AXIS2_PLACEMENT_3D('',#13153,#9866,#9867);
#9192=DIRECTION('',(0.,0.,1.));
#9193=DIRECTION('',(1.,0.,0.));
#9798=DIRECTION('',(1.,0.,0.));
#9799=DIRECTION('',(0.,0.,-1.));
#9800=DIRECTION('',(1.,0.,0.));
#9801=DIRECTION('',(0.,0.,-1.));
#9802=DIRECTION('',(1.,0.,0.));
#9803=DIRECTION('',(0.,0.,-1.));
#9804=DIRECTION('',(-1.,-3.26422297091706E-17,-2.83054210170864E-17));
#9805=DIRECTION('',(3.26422297091706E-17,-1.,0.));
#9806=DIRECTION('',(1.,-1.52525712114884E-12,-4.12654899649895E-17));
#9807=DIRECTION('',(1.52525712114884E-12,1.,0.));
#9808=DIRECTION('',(1.,-2.17614864727806E-17,1.88702806780578E-17));
#9809=DIRECTION('',(2.17614864727806E-17,1.,0.));
#9810=DIRECTION('',(1.,1.01718677511461E-12,2.49678409077823E-17));
#9811=DIRECTION('',(-1.01718677511461E-12,1.,0.));
#9812=DIRECTION('',(1.,-1.52525712114884E-12,-4.12654899649895E-17));
#9813=DIRECTION('',(1.52525712114884E-12,1.,0.));
#9814=DIRECTION('',(1.,1.52523423639394E-12,4.77734628794545E-17));
#9815=DIRECTION('',(-1.52523423639394E-12,1.,0.));
#9816=DIRECTION('',(1.,1.01718677511461E-12,2.49678409077823E-17));
#9817=DIRECTION('',(-1.01718677511461E-12,1.,0.));
#9818=DIRECTION('',(1.,-1.01703038514308E-12,2.74738847694775E-17));
#9819=DIRECTION('',(1.01703038514308E-12,1.,0.));
#9820=DIRECTION('',(-1.,0.,-1.0449157878825E-16));
#9821=DIRECTION('',(-1.0449157878825E-16,0.,1.));
#9822=DIRECTION('',(-1.,0.,-1.0449157878825E-16));
#9823=DIRECTION('',(-1.0449157878825E-16,0.,1.));
#9824=DIRECTION('',(1.,1.5253472309144E-12,1.6070040430106E-17));
#9825=DIRECTION('',(-1.5253472309144E-12,1.,0.));
#9826=DIRECTION('',(1.,-1.52537011566931E-12,-9.71439789292615E-18));
#9827=DIRECTION('',(1.52537011566931E-12,1.,0.));
#9828=DIRECTION('',(-1.,8.77687473398116E-18,8.62198870926304E-18));
#9829=DIRECTION('',(-8.77687473398116E-18,-1.,0.));
#9830=DIRECTION('',(1.,-1.28458696201097E-12,-2.92084213202575E-17));
#9831=DIRECTION('',(1.28458696201097E-12,1.,0.));
#9832=DIRECTION('',(-1.,0.,-1.11022302462516E-16));
#9833=DIRECTION('',(-1.11022302462516E-16,0.,1.));
#9834=DIRECTION('',(-1.,0.,-1.11022302462516E-16));
#9835=DIRECTION('',(-1.11022302462516E-16,0.,1.));
#9836=DIRECTION('',(1.,-1.28458696201097E-12,-2.92084213202575E-17));
#9837=DIRECTION('',(1.28458696201097E-12,1.,0.));
#9838=DIRECTION('',(-1.,0.,0.));
#9839=DIRECTION('',(0.,0.,1.));
#9840=DIRECTION('',(1.,-1.06677650229913E-10,1.79070058553459E-17));
#9841=DIRECTION('',(1.06677650229913E-10,1.,0.));
#9842=DIRECTION('',(1.,1.06677627345158E-10,-7.52576163854158E-18));
#9843=DIRECTION('',(-1.06677627345158E-10,1.,0.));
#9844=DIRECTION('',(-1.,0.,-1.04189432305107E-15));
#9845=DIRECTION('',(-1.04189432305107E-15,0.,1.));
#9846=DIRECTION('',(-1.,0.,0.));
#9847=DIRECTION('',(0.,0.,1.));
#9848=DIRECTION('',(-1.,0.,0.));
#9849=DIRECTION('',(0.,0.,1.));
#9850=DIRECTION('',(-1.,0.,-1.04189432305107E-15));
#9851=DIRECTION('',(-1.04189432305107E-15,0.,1.));
#9852=DIRECTION('',(-1.,0.,-1.04189432305107E-15));
#9853=DIRECTION('',(-1.04189432305107E-15,0.,1.));
#9854=DIRECTION('',(1.,3.57212507207529E-11,7.69107850575555E-18));
#9855=DIRECTION('',(-3.57212507207529E-11,1.,0.));
#9856=DIRECTION('',(1.,3.57212507207529E-11,7.69107850575555E-18));
#9857=DIRECTION('',(-3.57212507207529E-11,1.,0.));
#9858=DIRECTION('',(1.,-3.57214956501127E-11,-1.55638472566498E-17));
#9859=DIRECTION('',(3.57214956501127E-11,1.,0.));
#9860=DIRECTION('',(1.,1.13344866900787E-10,1.0907594486052E-16));
#9861=DIRECTION('',(-1.13344866900787E-10,1.,0.));
#9862=DIRECTION('',(1.,-1.13344929948816E-10,-1.04122921954656E-16));
#9863=DIRECTION('',(1.13344929948816E-10,1.,0.));
#9864=DIRECTION('',(1.,-1.13344929948816E-10,-1.04122921954656E-16));
#9865=DIRECTION('',(1.13344929948816E-10,1.,0.));
#9866=DIRECTION('',(-1.,0.,2.61228946970625E-17));
#9867=DIRECTION('',(2.61228946970625E-17,0.,1.));
#11098=CARTESIAN_POINT('',(0.,0.,0.));
#12971=CARTESIAN_POINT('',(-0.00525,0.,0.));
#12972=CARTESIAN_POINT('',(0.00525,0.,0.));
#12973=CARTESIAN_POINT('',(0.00525,0.,-0.0075));
#12974=CARTESIAN_POINT('',(-0.00525,0.,0.));
#12975=CARTESIAN_POINT('',(-0.00525,0.,-0.0075));
#12976=CARTESIAN_POINT('',(0.00525,-4.9439619065339E-19,-2.41993924898764E-18));
#12977=CARTESIAN_POINT('',(0.00525000000022048,1.9259841093292E-13,4.25226277214903E-19));
#12978=CARTESIAN_POINT('',(0.00525000000023268,0.00800000000074963,4.25226277214903E-19));
#12979=CARTESIAN_POINT('',(-0.00525,-5.50774703622636E-19,-8.67361737988404E-21));
#12980=CARTESIAN_POINT('',(-0.00525000000022048,1.92852798037857E-13,-1.01440902624871E-18));
#12981=CARTESIAN_POINT('',(-0.00525000000023269,0.0120000000007499,-1.01440902624871E-18));
#12982=CARTESIAN_POINT('',(0.00474999999987469,1.93361039494021E-13,4.45859022211667E-19));
#12983=CARTESIAN_POINT('',(0.00475000000055703,-1.93360444885966E-13,-1.48019874151438E-19));
#12984=CARTESIAN_POINT('',(0.00474999987540352,-1.74337662513279E-12,-0.00850000000012328));
#12985=CARTESIAN_POINT('',(0.00474999987527852,-4.86361310422452E-12,0.00850000000012328));
#12986=CARTESIAN_POINT('',(0.00475000000055704,-4.86361227985766E-12,0.00850000000024656));
#12987=CARTESIAN_POINT('',(0.00475000000055534,-0.00111264740275087,0.0084999999995846));
#12988=CARTESIAN_POINT('',(0.00475000000055195,-0.00333742350645399,0.00805742090693034));
#12989=CARTESIAN_POINT('',(0.00475000000054763,-0.00616690169649648,0.00616688297620523));
#12990=CARTESIAN_POINT('',(0.00475000000054475,-0.00805741556199689,0.00333749301577175));
#12991=CARTESIAN_POINT('',(0.00475000000054374,-0.00872129221938764,-1.60072261902693E-12));
#12992=CARTESIAN_POINT('',(0.00475000000054475,-0.00805741556077174,-0.00333749301872954));
#12993=CARTESIAN_POINT('',(0.00475000000054763,-0.00616690169423269,-0.00616688297846902));
#12994=CARTESIAN_POINT('',(0.00475000000055195,-0.00333742350349621,-0.00805742090815546));
#12995=CARTESIAN_POINT('',(0.00475000000055534,-0.00111264739963064,-0.00849999999999304));
#12996=CARTESIAN_POINT('',(0.00475000000055704,-1.7433859526852E-12,-0.00850000000024656));
#12997=CARTESIAN_POINT('',(-0.00474999999987469,1.93361391425766E-13,-1.00192510578618E-18));
#12998=CARTESIAN_POINT('',(-0.00424999999977952,1.92851057078383E-13,-6.6309546838198E-19));
#12999=CARTESIAN_POINT('',(-0.00424999999976732,0.0120000000007499,-6.6309546838198E-19));
#13000=CARTESIAN_POINT('',(-0.007263258046,0.,2.86039083864497E-51));
#13001=CARTESIAN_POINT('',(0.00425,-5.61175846058392E-12,-0.0085));
#13002=CARTESIAN_POINT('',(0.00425,-0.00111264740337218,-0.00849999999926542));
#13003=CARTESIAN_POINT('',(0.00425,-0.00333742350679297,-0.00805742090655498));
#13004=CARTESIAN_POINT('',(0.00425,-0.00616690169647487,-0.00616688297600855));
#13005=CARTESIAN_POINT('',(0.00425,-0.008057415561805,-0.00333749301594122));
#13006=CARTESIAN_POINT('',(0.00425,-0.00872129221928992,1.00565516758058E-12));
#13007=CARTESIAN_POINT('',(0.00425,-0.00805741556103531,0.00333749301779943));
#13008=CARTESIAN_POINT('',(0.00425,-0.00616690169505265,0.00616688297743077));
#13009=CARTESIAN_POINT('',(0.00425,-0.00333742350493477,0.00805742090732466));
#13010=CARTESIAN_POINT('',(0.00425,-0.0011126474014119,0.00849999999952203));
#13011=CARTESIAN_POINT('',(0.00425,-3.65148430959518E-12,0.0085));
#13012=CARTESIAN_POINT('',(0.00425,-2.88824233062088E-12,0.0085));
#13013=CARTESIAN_POINT('',(0.00425000037472148,-1.74337673725018E-12,-0.00850000000012328));
#13014=CARTESIAN_POINT('',(0.00425,0.,1.20303851022306E-18));
#13015=CARTESIAN_POINT('',(0.00425000000012531,1.93360815258866E-13,-2.80147189803738E-19));
#13016=CARTESIAN_POINT('',(0.00374999999977953,-2.71834574313571E-12,0.00800000000055703));
#13017=CARTESIAN_POINT('',(0.00374999999978272,-0.00209439510486201,0.00799999999979495));
#13018=CARTESIAN_POINT('',(0.00374999999978908,-0.00626651094914304,0.00626889299797267));
#13019=CARTESIAN_POINT('',(0.00374999999979305,-0.00886674452618622,-5.97131919231566E-13));
#13020=CARTESIAN_POINT('',(0.00374999999978908,-0.00626651094829869,-0.00626889299881671));
#13021=CARTESIAN_POINT('',(0.00374999999978272,-0.00209439510378449,-0.00800000000007704));
#13022=CARTESIAN_POINT('',(0.00374999999977953,-1.64082385457008E-12,-0.00800000000055703));
#13023=CARTESIAN_POINT('',(0.00374999987488976,-2.71834529339123E-12,0.00800000000027852));
#13024=CARTESIAN_POINT('',(0.00374999987488976,-1.64082717271973E-12,-0.00800000000040351));
#13025=CARTESIAN_POINT('',(0.00374999999977952,-1.92598860655761E-13,1.48862633905608E-19));
#13026=CARTESIAN_POINT('',(-0.00425,-5.50774703622636E-19,8.67361737988404E-21));
#13027=CARTESIAN_POINT('',(-0.00425000000022048,1.94006876112138E-13,-2.13954723767001E-19));
#13028=CARTESIAN_POINT('',(-0.00425000000020828,0.00949999999963698,-2.13954723767001E-19));
#13029=CARTESIAN_POINT('',(-0.007263258046,0.,2.83936039877452E-51));
#13030=CARTESIAN_POINT('',(0.001457106781,-5.28165502172604E-12,-0.008));
#13031=CARTESIAN_POINT('',(0.001457106781,-0.00209439510694832,-0.00799999999861726));
#13032=CARTESIAN_POINT('',(0.001457106781,-0.00626651094977711,-0.00626889299625425));
#13033=CARTESIAN_POINT('',(0.001457106781,-0.00886674452547288,1.0224280356647E-12));
#13034=CARTESIAN_POINT('',(0.001457106781,-0.00626651094833137,0.00626889299769943));
#13035=CARTESIAN_POINT('',(0.001457106781,-0.00209439510510336,0.00799999999910028));
#13036=CARTESIAN_POINT('',(0.001457106781,-3.43669111491311E-12,0.008));
#13037=CARTESIAN_POINT('',(0.001457106781,-2.7183457229373E-12,0.008));
#13038=CARTESIAN_POINT('',(0.001457107156,-2.28165122079125E-12,-0.008));
#13039=CARTESIAN_POINT('',(0.001457106781,0.,9.68154981406677E-19));
#13040=CARTESIAN_POINT('',(-0.00374999999987468,1.93364582630688E-13,-2.28558934437229E-19));
#13041=CARTESIAN_POINT('',(-0.00375,0.,0.));
#13042=CARTESIAN_POINT('',(-0.00374999987527851,-1.8459280570297E-12,-0.00899999999987672));
#13043=CARTESIAN_POINT('',(-0.00374999987527851,-1.22168301791654E-12,0.00899999999987672));
#13044=CARTESIAN_POINT('',(-0.00375000000055703,-1.22168309480298E-12,0.00899999999975343));
#13045=CARTESIAN_POINT('',(-0.00375000000055552,-0.00117809724617388,0.00899999999961883));
#13046=CARTESIAN_POINT('',(-0.00375000000055249,-0.00353374253293338,0.00853138684369092));
#13047=CARTESIAN_POINT('',(-0.00375000000054865,-0.0065296606176239,0.00652964080030454));
#13048=CARTESIAN_POINT('',(-0.00375000000054607,-0.00853138118227796,0.00353381613659912));
#13049=CARTESIAN_POINT('',(-0.00375000000054517,-0.00923430940871994,3.20239732450106E-13));
#13050=CARTESIAN_POINT('',(-0.00375000000054607,-0.00853138118252307,-0.00353381613600736));
#13051=CARTESIAN_POINT('',(-0.00375000000054865,-0.0065296606180768,-0.00652964079985164));
#13052=CARTESIAN_POINT('',(-0.00375000000055249,-0.00353374253352514,-0.00853138684344582));
#13053=CARTESIAN_POINT('',(-0.00375000000055552,-0.00117809724679812,-0.00899999999953711));
#13054=CARTESIAN_POINT('',(-0.00375000000055703,-1.845925958314E-12,-0.00899999999975343));
#13055=CARTESIAN_POINT('',(0.0014571067816285,-5.47396505703968E-13,6.65202876568241E-20));
#13056=CARTESIAN_POINT('',(0.00110355339071671,1.58556738773517E-17,0.00814644660952611));
#13057=CARTESIAN_POINT('',(0.00119611345182742,2.63259265651322E-16,0.00805388654805348));
#13058=CARTESIAN_POINT('',(0.00132620708739174,-1.64577341757993E-15,0.00799999999964119));
#13059=CARTESIAN_POINT('',(0.0014571067814045,1.67659206997871E-17,0.00799999999958255));
#13060=CARTESIAN_POINT('',(0.00110355330247001,-2.9115133713822E-12,0.0081464466976514));
#13061=CARTESIAN_POINT('',(0.00110355339071671,-1.6708634304086E-12,-0.00814644660952611));
#13062=CARTESIAN_POINT('',(0.00110355339048919,-0.00213273473648634,-0.00814644660922211));
#13063=CARTESIAN_POINT('',(0.00110355339003597,-0.0063812246085619,-0.0063836502643864));
#13064=CARTESIAN_POINT('',(0.00110355338975351,-0.00902905761052969,-6.87539018106074E-13));
#13065=CARTESIAN_POINT('',(0.00110355339003597,-0.00638122460953407,0.00638365026341459));
#13066=CARTESIAN_POINT('',(0.00110355339048919,-0.00213273473772698,0.00814644660889731));
#13067=CARTESIAN_POINT('',(0.00110355339071671,-2.91151058367133E-12,0.00814644660952611));
#13068=CARTESIAN_POINT('',(0.00110355330262237,-1.67086175802321E-12,-0.00814644669762802));
#13069=CARTESIAN_POINT('',(0.0014571067814045,-3.13787920007409E-17,-0.00799999999958255));
#13070=CARTESIAN_POINT('',(0.00132620708739174,-1.66845701558407E-15,-0.00799999999964119));
#13071=CARTESIAN_POINT('',(0.00119611345182742,2.65760905900004E-16,-0.00805388654805348));
#13072=CARTESIAN_POINT('',(0.00110355339071671,4.46112367465754E-17,-0.00814644660952611));
#13073=CARTESIAN_POINT('',(0.0014571067816285,5.47397208070073E-13,-5.45798719985721E-19));
#13074=CARTESIAN_POINT('',(0.00110355339112794,0.,-1.04204690494148E-15));
#13075=CARTESIAN_POINT('',(-0.007263258046,0.,0.));
#13076=CARTESIAN_POINT('',(-0.003116025404,-3.86627750427725E-12,0.009));
#13077=CARTESIAN_POINT('',(-0.003116025404,-0.00117809724855378,0.0089999999994939));
#13078=CARTESIAN_POINT('',(-0.003116025404,-0.00353374253463681,0.00853138684304964));
#13079=CARTESIAN_POINT('',(-0.003116025404,-0.00652966061829104,0.00652964079963258));
#13080=CARTESIAN_POINT('',(-0.003116025404,-0.00853138118227268,0.00353381613649351));
#13081=CARTESIAN_POINT('',(-0.003116025404,-0.00923430940865992,1.06481072844012E-12));
#13082=CARTESIAN_POINT('',(-0.003116025404,-0.00853138118308765,-0.003533816134526));
#13083=CARTESIAN_POINT('',(-0.003116025404,-0.00652966061979692,-0.0065296407981267));
#13084=CARTESIAN_POINT('',(-0.003116025404,-0.00353374253660432,-0.00853138684223469));
#13085=CARTESIAN_POINT('',(-0.003116025404,-0.00117809725062936,-0.00899999999922221));
#13086=CARTESIAN_POINT('',(-0.003116025404,-5.9418618994418E-12,-0.009));
#13087=CARTESIAN_POINT('',(-0.00311602552873704,-1.84592937600593E-12,-0.00899999999997601));
#13088=CARTESIAN_POINT('',(-0.00311602552873704,1.12499936185184E-12,0.00899999999997601));
#13089=CARTESIAN_POINT('',(-0.003116025404,0.,0.));
#13090=CARTESIAN_POINT('',(0.00925000000025689,0.,-1.03355916846639E-15));
#13091=CARTESIAN_POINT('',(0.000896446609127943,0.,-1.04226268832191E-15));
#13092=CARTESIAN_POINT('',(0.000896446947516299,-2.38248677279272E-12,-0.00835355305274167));
#13093=CARTESIAN_POINT('',(0.000896446609127934,-2.83848445413882E-12,0.00835355339112793));
#13094=CARTESIAN_POINT('',(0.000896446609127957,-5.51507340218912E-12,-0.00835355339113002));
#13095=CARTESIAN_POINT('',(0.000896446609127957,-0.00109347758700829,-0.0083535533904081));
#13096=CARTESIAN_POINT('',(0.000896446609127956,-0.00327992299444752,-0.00791859949855468));
#13097=CARTESIAN_POINT('',(0.000896446609127955,-0.00606065206815843,-0.00606063367022831));
#13098=CARTESIAN_POINT('',(0.000896446609127951,-0.00791859424588842,-0.00327999130602281));
#13099=CARTESIAN_POINT('',(0.000896446609127948,-0.00857103296393836,9.87285581686735E-13));
#13100=CARTESIAN_POINT('',(0.000896446609127945,-0.00791859424513199,0.00327999130784692));
#13101=CARTESIAN_POINT('',(0.000896446609127942,-0.00606065206676072,0.00606063367162394));
#13102=CARTESIAN_POINT('',(0.00089644660912794,-0.00327992299262134,0.00791859949930901));
#13103=CARTESIAN_POINT('',(0.000896446609127939,-0.00109347758508179,0.00835355339065819));
#13104=CARTESIAN_POINT('',(0.000896446609127939,-3.58857283965566E-12,0.00835355339112793));
#13105=CARTESIAN_POINT('',(-0.00311602540366083,1.89369138590977E-13,4.60164670987285E-19));
#13106=CARTESIAN_POINT('',(-0.00311602540347409,-2.08135904343245E-17,0.00899999999995202));
#13107=CARTESIAN_POINT('',(-0.00276695955312565,-2.17671273402248E-15,0.00899999999988684));
#13108=CARTESIAN_POINT('',(-0.00242453292500672,-2.5821733949979E-16,0.00880229989405671));
#13109=CARTESIAN_POINT('',(-0.00224999999965417,-1.04806440198648E-18,0.0085000000001643));
#13110=CARTESIAN_POINT('',(-0.00224999987482708,-1.83738466424475E-19,0.00850000000008215));
#13111=CARTESIAN_POINT('',(-0.00224999999965417,2.2030464917804E-13,4.66825340357479E-19));
#13112=CARTESIAN_POINT('',(-0.00224999987482708,-1.74337942337899E-12,-0.00850000000008215));
#13113=CARTESIAN_POINT('',(-0.00224999999965417,-1.44542388119606E-17,-0.0085000000001643));
#13114=CARTESIAN_POINT('',(-0.00242453292500672,-2.56372140876474E-16,-0.00880229989405671));
#13115=CARTESIAN_POINT('',(-0.00276695955312565,-2.15760081618848E-15,-0.00899999999988684));
#13116=CARTESIAN_POINT('',(-0.00311602540347409,1.49516727692217E-17,-0.00899999999995202));
#13117=CARTESIAN_POINT('',(-0.00311602540366083,-1.89369495587902E-13,-4.56753702428283E-19));
#13118=CARTESIAN_POINT('',(-0.00224999999965417,-1.74337645012797E-12,-0.0085000000001643));
#13119=CARTESIAN_POINT('',(-0.00224999999969392,-0.00111264739985699,-0.00849999999996493));
#13120=CARTESIAN_POINT('',(-0.00224999999977339,-0.00333742350419627,-0.00805742090804886));
#13121=CARTESIAN_POINT('',(-0.00224999999987446,-0.00616690169538636,-0.00616688297774479));
#13122=CARTESIAN_POINT('',(-0.002249999999942,-0.00805741556187121,-0.00333749301710294));
#13123=CARTESIAN_POINT('',(-0.00224999999996571,-0.00872129221981244,8.94381676439934E-13));
#13124=CARTESIAN_POINT('',(-0.002249999999942,-0.00805741556118667,0.00333749301875555));
#13125=CARTESIAN_POINT('',(-0.00224999999987446,-0.00616690169412152,0.00616688297900963));
#13126=CARTESIAN_POINT('',(-0.00224999999977339,-0.00333742350254365,0.00805742090873338));
#13127=CARTESIAN_POINT('',(-0.00224999999969392,-0.00111264739811362,0.00850000000019314));
#13128=CARTESIAN_POINT('',(-0.00224999999965417,-1.35791309261817E-17,0.0085000000001643));
#13129=CARTESIAN_POINT('',(0.000542893218371495,5.47403523416524E-13,1.10783975326665E-19));
#13130=CARTESIAN_POINT('',(0.000896446609283292,-1.46288588890009E-17,0.0083535533904739));
#13131=CARTESIAN_POINT('',(0.000803886548172581,-5.03456191566966E-16,0.00844611345194653));
#13132=CARTESIAN_POINT('',(0.00067379291260826,-1.94773245151004E-15,0.00850000000035882));
#13133=CARTESIAN_POINT('',(0.000542893218595496,1.69082711704543E-17,0.00850000000041746));
#13134=CARTESIAN_POINT('',(0.000542893093797748,-2.12500021499821E-12,0.00850000000020873));
#13135=CARTESIAN_POINT('',(0.000542893218595496,-2.12499836668962E-12,0.00850000000041746));
#13136=CARTESIAN_POINT('',(0.000542893218721609,-0.00111264740011923,0.00850000000006764));
#13137=CARTESIAN_POINT('',(0.000542893218973776,-0.00333742350416026,0.00805742090796045));
#13138=CARTESIAN_POINT('',(0.000542893219294483,-0.00616690169492879,0.00616688297771508));
#13139=CARTESIAN_POINT('',(0.000542893219508763,-0.00805741556119902,0.00333749301739052));
#13140=CARTESIAN_POINT('',(0.00054289321958401,-0.00872129221924304,-1.95784323807277E-13));
#13141=CARTESIAN_POINT('',(0.000542893219508763,-0.00805741556104918,-0.00333749301775226));
#13142=CARTESIAN_POINT('',(0.000542893219294483,-0.00616690169465192,-0.00616688297799194));
#13143=CARTESIAN_POINT('',(0.000542893218973777,-0.00333742350379851,-0.00805742090811029));
#13144=CARTESIAN_POINT('',(0.000542893218721609,-0.00111264739973761,-0.0085000000001176));
#13145=CARTESIAN_POINT('',(0.000542893218595496,-1.74337804822321E-12,-0.00850000000041746));
#13146=CARTESIAN_POINT('',(0.000542893093922748,-1.7433764476282E-12,-0.00850000000020873));
#13147=CARTESIAN_POINT('',(0.000542893218595496,1.61471761803093E-18,-0.00850000000041746));
#13148=CARTESIAN_POINT('',(0.000673792912608261,-1.96176775230103E-15,-0.00850000000035882));
#13149=CARTESIAN_POINT('',(0.000803886548172583,-5.16138536658815E-16,-0.00844611345194653));
#13150=CARTESIAN_POINT('',(0.000896446609283294,-2.59491966845735E-17,-0.0083535533904739));
#13151=CARTESIAN_POINT('',(0.000542893218371494,-5.47404119942789E-13,5.87721542220263E-20));
#13152=CARTESIAN_POINT('',(0.000542893218595497,-5.47404119968178E-13,5.87721541987024E-20));
#13153=CARTESIAN_POINT('',(-0.007263258046,0.,2.44324620272917E-53));
#18809=MECHANICAL_DESIGN_GEOMETRIC_PRESENTATION_REPRESENTATION('',(#8175),#18810);
#18810=(
GEOMETRIC_REPRESENTATION_CONTEXT(3)
GLOBAL_UNCERTAINTY_ASSIGNED_CONTEXT((#18817))
GLOBAL_UNIT_ASSIGNED_CONTEXT((#18826,#18825,#18824))
REPRESENTATION_CONTEXT('MAS-697','TOP_LEVEL_ASSEMBLY_PART')
);
#18812=(
GEOMETRIC_REPRESENTATION_CONTEXT(3)
GLOBAL_UNCERTAINTY_ASSIGNED_CONTEXT((#18819))
GLOBAL_UNIT_ASSIGNED_CONTEXT((#18826,#18825,#18824))
REPRESENTATION_CONTEXT('endcap2__ DE    22113','COMPONENT_PART')
);
#18817=UNCERTAINTY_MEASURE_WITH_UNIT(LENGTH_MEASURE(1.E-8),#18826,
'DISTANCE_ACCURACY_VALUE','Maximum Tolerance applied to model');
#18819=UNCERTAINTY_MEASURE_WITH_UNIT(LENGTH_MEASURE(2.E-5),#18826,
'DISTANCE_ACCURACY_VALUE','Maximum Tolerance applied to model');
#18824=(
NAMED_UNIT(*)
SI_UNIT($,.STERADIAN.)
SOLID_ANGLE_UNIT()
);
#18825=(
NAMED_UNIT(*)
PLANE_ANGLE_UNIT()
SI_UNIT($,.RADIAN.)
);
#18826=(
LENGTH_UNIT()
NAMED_UNIT(*)
SI_UNIT($,.METRE.)
);
#18830=PRODUCT_DEFINITION_SHAPE('','',#18842);
#18842=PRODUCT_DEFINITION('','',#18856,#18849);
#18849=PRODUCT_DEFINITION_CONTEXT('',#18890,'design');
#18856=PRODUCT_DEFINITION_FORMATION_WITH_SPECIFIED_SOURCE('','',#18870,
 .NOT_KNOWN.);
#18870=PRODUCT('endcap2__ DE    22113','endcap2__ DE    22113',
'endcap2__ DE    22113',(#18884));
#18884=PRODUCT_CONTEXT('',#18890,'mechanical');
#18890=APPLICATION_CONTEXT('managed model based 3d engineering');
ENDSEC;
END-ISO-10303-21;
